ISO-10303-21;
HEADER;
/* Generated by software containing ST-Developer
 * from STEP Tools, Inc. (www.steptools.com) 
 */

FILE_DESCRIPTION(
/* description */ ('Cam-driven reciprocating slide'),
/* implementation_level */ '2;1');

FILE_NAME(
/* name */ 'Cap Screw - M5x20.step',
/* time_stamp */ '2026-10-28T03:25:20-07:00',
/* author */ (''),
/* organization */ (''),
/* preprocessor_version */ 'ST-DEVELOPER v20.2',
/* originating_system */ 'Autodesk Translation Framework v15.17.0.0',
/* authorisation */ '');

FILE_SCHEMA (('AUTOMOTIVE_DESIGN { 1 0 10303 214 3 1 1 }'));
ENDSEC;

DATA;
#10=MECHANICAL_DESIGN_GEOMETRIC_PRESENTATION_REPRESENTATION('',(#447),#13277);
#11=ORIENTED_CLOSED_SHELL('',*,#6424,.F.);
#14=BREP_WITH_VOIDS('Body1',#6423,(#11));
#319=CONICAL_SURFACE('',#7285,0.4,0.785398163397448);
#320=CONICAL_SURFACE('',#7289,0.41,0.785398163397448);
#321=CONICAL_SURFACE('',#7293,0.26,0.463647609000806);
#322=CONICAL_SURFACE('',#7297,0.225,0.785398163397448);
#366=SHAPE_REPRESENTATION_RELATIONSHIP('SRR','None',#13460,#403);
#403=ADVANCED_BREP_SHAPE_REPRESENTATION('',(#14),#13255);
#447=STYLED_ITEM('',(#13727),#14);
#627=FACE_BOUND('',#1604,.T.);
#780=PLANE('',#7283);
#781=PLANE('',#7291);
#782=PLANE('',#7299);
#783=PLANE('',#7300);
#784=PLANE('',#7301);
#785=PLANE('',#7302);
#786=PLANE('',#7303);
#787=PLANE('',#7304);
#788=PLANE('',#7305);
#789=PLANE('',#7306);
#790=PLANE('',#7307);
#1100=FACE_OUTER_BOUND('',#1599,.T.);
#1101=FACE_OUTER_BOUND('',#1600,.T.);
#1102=FACE_OUTER_BOUND('',#1601,.T.);
#1103=FACE_OUTER_BOUND('',#1602,.T.);
#1104=FACE_OUTER_BOUND('',#1603,.T.);
#1105=FACE_OUTER_BOUND('',#1605,.T.);
#1106=FACE_OUTER_BOUND('',#1606,.T.);
#1107=FACE_OUTER_BOUND('',#1607,.T.);
#1108=FACE_OUTER_BOUND('',#1608,.T.);
#1109=FACE_OUTER_BOUND('',#1609,.T.);
#1110=FACE_OUTER_BOUND('',#1610,.T.);
#1111=FACE_OUTER_BOUND('',#1611,.T.);
#1112=FACE_OUTER_BOUND('',#1612,.T.);
#1113=FACE_OUTER_BOUND('',#1613,.T.);
#1114=FACE_OUTER_BOUND('',#1614,.T.);
#1115=FACE_OUTER_BOUND('',#1615,.T.);
#1116=FACE_OUTER_BOUND('',#1616,.T.);
#1599=EDGE_LOOP('',(#5206));
#1600=EDGE_LOOP('',(#5207,#5208,#5209,#5210));
#1601=EDGE_LOOP('',(#5211,#5212,#5213,#5214));
#1602=EDGE_LOOP('',(#5215,#5216,#5217,#5218));
#1603=EDGE_LOOP('',(#5219));
#1604=EDGE_LOOP('',(#5220));
#1605=EDGE_LOOP('',(#5221,#5222,#5223,#5224));
#1606=EDGE_LOOP('',(#5225,#5226,#5227,#5228));
#1607=EDGE_LOOP('',(#5229,#5230,#5231,#5232));
#1608=EDGE_LOOP('',(#5233));
#1609=EDGE_LOOP('',(#5234,#5235,#5236,#5237));
#1610=EDGE_LOOP('',(#5238,#5239,#5240,#5241));
#1611=EDGE_LOOP('',(#5242,#5243,#5244,#5245));
#1612=EDGE_LOOP('',(#5246,#5247,#5248,#5249));
#1613=EDGE_LOOP('',(#5250,#5251,#5252,#5253));
#1614=EDGE_LOOP('',(#5254,#5255,#5256,#5257));
#1615=EDGE_LOOP('',(#5258,#5259,#5260,#5261,#5262,#5263));
#1616=EDGE_LOOP('',(#5264,#5265,#5266,#5267,#5268,#5269));
#2048=LINE('',#12361,#2487);
#2049=LINE('',#12365,#2488);
#2050=LINE('',#12369,#2489);
#2051=LINE('',#12376,#2490);
#2052=LINE('',#12380,#2491);
#2053=LINE('',#12384,#2492);
#2054=LINE('',#12389,#2493);
#2055=LINE('',#12391,#2494);
#2056=LINE('',#12393,#2495);
#2057=LINE('',#12394,#2496);
#2058=LINE('',#12397,#2497);
#2059=LINE('',#12399,#2498);
#2060=LINE('',#12400,#2499);
#2061=LINE('',#12403,#2500);
#2062=LINE('',#12405,#2501);
#2063=LINE('',#12406,#2502);
#2064=LINE('',#12409,#2503);
#2065=LINE('',#12411,#2504);
#2066=LINE('',#12412,#2505);
#2067=LINE('',#12415,#2506);
#2068=LINE('',#12417,#2507);
#2069=LINE('',#12418,#2508);
#2070=LINE('',#12420,#2509);
#2071=LINE('',#12421,#2510);
#2487=VECTOR('',#8752,0.4);
#2488=VECTOR('',#8757,0.425);
#2489=VECTOR('',#8762,0.41);
#2490=VECTOR('',#8771,0.26);
#2491=VECTOR('',#8776,0.25);
#2492=VECTOR('',#8781,0.225);
#2493=VECTOR('',#8786,1.);
#2494=VECTOR('',#8787,1.);
#2495=VECTOR('',#8788,1.);
#2496=VECTOR('',#8789,1.);
#2497=VECTOR('',#8792,1.);
#2498=VECTOR('',#8793,1.);
#2499=VECTOR('',#8794,1.);
#2500=VECTOR('',#8797,1.);
#2501=VECTOR('',#8798,1.);
#2502=VECTOR('',#8799,1.);
#2503=VECTOR('',#8802,1.);
#2504=VECTOR('',#8803,1.);
#2505=VECTOR('',#8804,1.);
#2506=VECTOR('',#8807,1.);
#2507=VECTOR('',#8808,1.);
#2508=VECTOR('',#8809,1.);
#2509=VECTOR('',#8812,1.);
#2510=VECTOR('',#8813,1.);
#2916=CIRCLE('',#7284,0.375);
#2917=CIRCLE('',#7286,0.425);
#2918=CIRCLE('',#7288,0.425);
#2919=CIRCLE('',#7290,0.395);
#2920=CIRCLE('',#7292,0.27);
#2921=CIRCLE('',#7294,0.24505);
#2922=CIRCLE('',#7296,0.24505);
#2923=CIRCLE('',#7298,0.2);
#3333=VERTEX_POINT('',#12356);
#3334=VERTEX_POINT('',#12359);
#3335=VERTEX_POINT('',#12363);
#3336=VERTEX_POINT('',#12367);
#3337=VERTEX_POINT('',#12371);
#3338=VERTEX_POINT('',#12374);
#3339=VERTEX_POINT('',#12378);
#3340=VERTEX_POINT('',#12382);
#3341=VERTEX_POINT('',#12387);
#3342=VERTEX_POINT('',#12388);
#3343=VERTEX_POINT('',#12390);
#3344=VERTEX_POINT('',#12392);
#3345=VERTEX_POINT('',#12396);
#3346=VERTEX_POINT('',#12398);
#3347=VERTEX_POINT('',#12402);
#3348=VERTEX_POINT('',#12404);
#3349=VERTEX_POINT('',#12408);
#3350=VERTEX_POINT('',#12410);
#3351=VERTEX_POINT('',#12414);
#3352=VERTEX_POINT('',#12416);
#3993=EDGE_CURVE('',#3333,#3333,#2916,.T.);
#3994=EDGE_CURVE('',#3334,#3334,#2917,.T.);
#3995=EDGE_CURVE('',#3334,#3333,#2048,.T.);
#3996=EDGE_CURVE('',#3335,#3335,#2918,.T.);
#3997=EDGE_CURVE('',#3335,#3334,#2049,.T.);
#3998=EDGE_CURVE('',#3336,#3336,#2919,.T.);
#3999=EDGE_CURVE('',#3336,#3335,#2050,.T.);
#4000=EDGE_CURVE('',#3337,#3337,#2920,.T.);
#4001=EDGE_CURVE('',#3338,#3338,#2921,.F.);
#4002=EDGE_CURVE('',#3338,#3337,#2051,.T.);
#4003=EDGE_CURVE('',#3339,#3339,#2922,.F.);
#4004=EDGE_CURVE('',#3339,#3338,#2052,.T.);
#4005=EDGE_CURVE('',#3340,#3340,#2923,.T.);
#4006=EDGE_CURVE('',#3340,#3339,#2053,.T.);
#4007=EDGE_CURVE('',#3341,#3342,#2054,.T.);
#4008=EDGE_CURVE('',#3342,#3343,#2055,.T.);
#4009=EDGE_CURVE('',#3343,#3344,#2056,.T.);
#4010=EDGE_CURVE('',#3341,#3344,#2057,.T.);
#4011=EDGE_CURVE('',#3342,#3345,#2058,.T.);
#4012=EDGE_CURVE('',#3345,#3346,#2059,.T.);
#4013=EDGE_CURVE('',#3346,#3343,#2060,.T.);
#4014=EDGE_CURVE('',#3345,#3347,#2061,.T.);
#4015=EDGE_CURVE('',#3347,#3348,#2062,.T.);
#4016=EDGE_CURVE('',#3348,#3346,#2063,.T.);
#4017=EDGE_CURVE('',#3347,#3349,#2064,.T.);
#4018=EDGE_CURVE('',#3349,#3350,#2065,.T.);
#4019=EDGE_CURVE('',#3350,#3348,#2066,.T.);
#4020=EDGE_CURVE('',#3349,#3351,#2067,.T.);
#4021=EDGE_CURVE('',#3351,#3352,#2068,.T.);
#4022=EDGE_CURVE('',#3352,#3350,#2069,.T.);
#4023=EDGE_CURVE('',#3351,#3341,#2070,.T.);
#4024=EDGE_CURVE('',#3344,#3352,#2071,.T.);
#5206=ORIENTED_EDGE('',*,*,#3993,.F.);
#5207=ORIENTED_EDGE('',*,*,#3994,.F.);
#5208=ORIENTED_EDGE('',*,*,#3995,.T.);
#5209=ORIENTED_EDGE('',*,*,#3993,.T.);
#5210=ORIENTED_EDGE('',*,*,#3995,.F.);
#5211=ORIENTED_EDGE('',*,*,#3996,.F.);
#5212=ORIENTED_EDGE('',*,*,#3997,.T.);
#5213=ORIENTED_EDGE('',*,*,#3994,.T.);
#5214=ORIENTED_EDGE('',*,*,#3997,.F.);
#5215=ORIENTED_EDGE('',*,*,#3998,.F.);
#5216=ORIENTED_EDGE('',*,*,#3999,.T.);
#5217=ORIENTED_EDGE('',*,*,#3996,.T.);
#5218=ORIENTED_EDGE('',*,*,#3999,.F.);
#5219=ORIENTED_EDGE('',*,*,#3998,.T.);
#5220=ORIENTED_EDGE('',*,*,#4000,.F.);
#5221=ORIENTED_EDGE('',*,*,#4001,.F.);
#5222=ORIENTED_EDGE('',*,*,#4002,.T.);
#5223=ORIENTED_EDGE('',*,*,#4000,.T.);
#5224=ORIENTED_EDGE('',*,*,#4002,.F.);
#5225=ORIENTED_EDGE('',*,*,#4003,.F.);
#5226=ORIENTED_EDGE('',*,*,#4004,.T.);
#5227=ORIENTED_EDGE('',*,*,#4001,.T.);
#5228=ORIENTED_EDGE('',*,*,#4004,.F.);
#5229=ORIENTED_EDGE('',*,*,#4005,.F.);
#5230=ORIENTED_EDGE('',*,*,#4006,.T.);
#5231=ORIENTED_EDGE('',*,*,#4003,.T.);
#5232=ORIENTED_EDGE('',*,*,#4006,.F.);
#5233=ORIENTED_EDGE('',*,*,#4005,.T.);
#5234=ORIENTED_EDGE('',*,*,#4007,.T.);
#5235=ORIENTED_EDGE('',*,*,#4008,.T.);
#5236=ORIENTED_EDGE('',*,*,#4009,.T.);
#5237=ORIENTED_EDGE('',*,*,#4010,.F.);
#5238=ORIENTED_EDGE('',*,*,#4011,.T.);
#5239=ORIENTED_EDGE('',*,*,#4012,.T.);
#5240=ORIENTED_EDGE('',*,*,#4013,.T.);
#5241=ORIENTED_EDGE('',*,*,#4008,.F.);
#5242=ORIENTED_EDGE('',*,*,#4014,.T.);
#5243=ORIENTED_EDGE('',*,*,#4015,.T.);
#5244=ORIENTED_EDGE('',*,*,#4016,.T.);
#5245=ORIENTED_EDGE('',*,*,#4012,.F.);
#5246=ORIENTED_EDGE('',*,*,#4017,.T.);
#5247=ORIENTED_EDGE('',*,*,#4018,.T.);
#5248=ORIENTED_EDGE('',*,*,#4019,.T.);
#5249=ORIENTED_EDGE('',*,*,#4015,.F.);
#5250=ORIENTED_EDGE('',*,*,#4020,.T.);
#5251=ORIENTED_EDGE('',*,*,#4021,.T.);
#5252=ORIENTED_EDGE('',*,*,#4022,.T.);
#5253=ORIENTED_EDGE('',*,*,#4018,.F.);
#5254=ORIENTED_EDGE('',*,*,#4023,.T.);
#5255=ORIENTED_EDGE('',*,*,#4010,.T.);
#5256=ORIENTED_EDGE('',*,*,#4024,.T.);
#5257=ORIENTED_EDGE('',*,*,#4021,.F.);
#5258=ORIENTED_EDGE('',*,*,#4023,.F.);
#5259=ORIENTED_EDGE('',*,*,#4020,.F.);
#5260=ORIENTED_EDGE('',*,*,#4017,.F.);
#5261=ORIENTED_EDGE('',*,*,#4014,.F.);
#5262=ORIENTED_EDGE('',*,*,#4011,.F.);
#5263=ORIENTED_EDGE('',*,*,#4007,.F.);
#5264=ORIENTED_EDGE('',*,*,#4024,.F.);
#5265=ORIENTED_EDGE('',*,*,#4009,.F.);
#5266=ORIENTED_EDGE('',*,*,#4013,.F.);
#5267=ORIENTED_EDGE('',*,*,#4016,.F.);
#5268=ORIENTED_EDGE('',*,*,#4019,.F.);
#5269=ORIENTED_EDGE('',*,*,#4022,.F.);
#5971=CYLINDRICAL_SURFACE('',#7287,0.425);
#5972=CYLINDRICAL_SURFACE('',#7295,0.24505);
#6218=ADVANCED_FACE('',(#1100),#780,.T.);
#6219=ADVANCED_FACE('',(#1101),#319,.T.);
#6220=ADVANCED_FACE('',(#1102),#5971,.T.);
#6221=ADVANCED_FACE('',(#1103),#320,.T.);
#6222=ADVANCED_FACE('',(#1104,#627),#781,.T.);
#6223=ADVANCED_FACE('',(#1105),#321,.T.);
#6224=ADVANCED_FACE('',(#1106),#5972,.T.);
#6225=ADVANCED_FACE('',(#1107),#322,.T.);
#6226=ADVANCED_FACE('',(#1108),#782,.T.);
#6227=ADVANCED_FACE('',(#1109),#783,.F.);
#6228=ADVANCED_FACE('',(#1110),#784,.F.);
#6229=ADVANCED_FACE('',(#1111),#785,.F.);
#6230=ADVANCED_FACE('',(#1112),#786,.F.);
#6231=ADVANCED_FACE('',(#1113),#787,.F.);
#6232=ADVANCED_FACE('',(#1114),#788,.F.);
#6233=ADVANCED_FACE('',(#1115),#789,.F.);
#6234=ADVANCED_FACE('',(#1116),#790,.F.);
#6423=CLOSED_SHELL('',(#6218,#6219,#6220,#6221,#6222,#6223,#6224,#6225,
#6226));
#6424=CLOSED_SHELL('',(#6227,#6228,#6229,#6230,#6231,#6232,#6233,#6234));
#7282=AXIS2_PLACEMENT_3D('',#12354,#8742,#8743);
#7283=AXIS2_PLACEMENT_3D('',#12355,#8744,#8745);
#7284=AXIS2_PLACEMENT_3D('',#12357,#8746,#8747);
#7285=AXIS2_PLACEMENT_3D('',#12358,#8748,#8749);
#7286=AXIS2_PLACEMENT_3D('',#12360,#8750,#8751);
#7287=AXIS2_PLACEMENT_3D('',#12362,#8753,#8754);
#7288=AXIS2_PLACEMENT_3D('',#12364,#8755,#8756);
#7289=AXIS2_PLACEMENT_3D('',#12366,#8758,#8759);
#7290=AXIS2_PLACEMENT_3D('',#12368,#8760,#8761);
#7291=AXIS2_PLACEMENT_3D('',#12370,#8763,#8764);
#7292=AXIS2_PLACEMENT_3D('',#12372,#8765,#8766);
#7293=AXIS2_PLACEMENT_3D('',#12373,#8767,#8768);
#7294=AXIS2_PLACEMENT_3D('',#12375,#8769,#8770);
#7295=AXIS2_PLACEMENT_3D('',#12377,#8772,#8773);
#7296=AXIS2_PLACEMENT_3D('',#12379,#8774,#8775);
#7297=AXIS2_PLACEMENT_3D('',#12381,#8777,#8778);
#7298=AXIS2_PLACEMENT_3D('',#12383,#8779,#8780);
#7299=AXIS2_PLACEMENT_3D('',#12385,#8782,#8783);
#7300=AXIS2_PLACEMENT_3D('',#12386,#8784,#8785);
#7301=AXIS2_PLACEMENT_3D('',#12395,#8790,#8791);
#7302=AXIS2_PLACEMENT_3D('',#12401,#8795,#8796);
#7303=AXIS2_PLACEMENT_3D('',#12407,#8800,#8801);
#7304=AXIS2_PLACEMENT_3D('',#12413,#8805,#8806);
#7305=AXIS2_PLACEMENT_3D('',#12419,#8810,#8811);
#7306=AXIS2_PLACEMENT_3D('',#12422,#8814,#8815);
#7307=AXIS2_PLACEMENT_3D('',#12423,#8816,#8817);
#8742=DIRECTION('axis',(0.,0.,1.));
#8743=DIRECTION('refdir',(1.,0.,0.));
#8744=DIRECTION('center_axis',(0.,1.,0.));
#8745=DIRECTION('ref_axis',(0.,0.,1.));
#8746=DIRECTION('center_axis',(0.,-1.,0.));
#8747=DIRECTION('ref_axis',(1.,0.,0.));
#8748=DIRECTION('center_axis',(0.,-1.,0.));
#8749=DIRECTION('ref_axis',(1.,0.,0.));
#8750=DIRECTION('center_axis',(0.,-1.,0.));
#8751=DIRECTION('ref_axis',(1.,0.,0.));
#8752=DIRECTION('',(0.707106781186548,0.707106781186547,8.65956056235493E-17));
#8753=DIRECTION('center_axis',(0.,-1.,0.));
#8754=DIRECTION('ref_axis',(1.,0.,0.));
#8755=DIRECTION('center_axis',(0.,-1.,0.));
#8756=DIRECTION('ref_axis',(1.,0.,0.));
#8757=DIRECTION('',(0.,1.,0.));
#8758=DIRECTION('center_axis',(0.,1.,0.));
#8759=DIRECTION('ref_axis',(1.,0.,0.));
#8760=DIRECTION('center_axis',(0.,-1.,0.));
#8761=DIRECTION('ref_axis',(1.,0.,0.));
#8762=DIRECTION('',(-0.707106781186547,0.707106781186548,-8.65956056235493E-17));
#8763=DIRECTION('center_axis',(0.,-1.,0.));
#8764=DIRECTION('ref_axis',(0.,0.,-1.));
#8765=DIRECTION('center_axis',(0.,-1.,0.));
#8766=DIRECTION('ref_axis',(1.,0.,0.));
#8767=DIRECTION('center_axis',(0.,1.,0.));
#8768=DIRECTION('ref_axis',(1.,0.,0.));
#8769=DIRECTION('center_axis',(0.,1.,0.));
#8770=DIRECTION('ref_axis',(1.,0.,0.));
#8771=DIRECTION('',(-0.447213595499958,0.894427190999916,-5.47678698264203E-17));
#8772=DIRECTION('center_axis',(0.,-1.,0.));
#8773=DIRECTION('ref_axis',(1.,0.,0.));
#8774=DIRECTION('center_axis',(0.,1.,0.));
#8775=DIRECTION('ref_axis',(1.,0.,0.));
#8776=DIRECTION('',(0.,1.,0.));
#8777=DIRECTION('center_axis',(0.,1.,0.));
#8778=DIRECTION('ref_axis',(1.,0.,0.));
#8779=DIRECTION('center_axis',(0.,-1.,0.));
#8780=DIRECTION('ref_axis',(1.,0.,0.));
#8781=DIRECTION('',(-0.707106781186547,0.707106781186548,-8.65956056235493E-17));
#8782=DIRECTION('center_axis',(0.,-1.,0.));
#8783=DIRECTION('ref_axis',(0.,0.,-1.));
#8784=DIRECTION('center_axis',(0.866025403784439,0.,-0.5));
#8785=DIRECTION('ref_axis',(0.5,0.,0.866025403784439));
#8786=DIRECTION('',(-0.5,0.,-0.866025403784439));
#8787=DIRECTION('',(0.,-1.,0.));
#8788=DIRECTION('',(0.5,0.,0.866025403784439));
#8789=DIRECTION('',(0.,-1.,0.));
#8790=DIRECTION('center_axis',(1.20185167898973E-16,0.,-1.));
#8791=DIRECTION('ref_axis',(1.,0.,1.20185167898973E-16));
#8792=DIRECTION('',(-1.,0.,-1.20185167898973E-16));
#8793=DIRECTION('',(0.,-1.,0.));
#8794=DIRECTION('',(1.,0.,1.20185167898973E-16));
#8795=DIRECTION('center_axis',(-0.866025403784439,0.,-0.5));
#8796=DIRECTION('ref_axis',(0.5,0.,-0.866025403784439));
#8797=DIRECTION('',(-0.5,0.,0.866025403784439));
#8798=DIRECTION('',(0.,-1.,0.));
#8799=DIRECTION('',(0.5,0.,-0.866025403784439));
#8800=DIRECTION('center_axis',(-0.866025403784439,0.,0.5));
#8801=DIRECTION('ref_axis',(-0.5,0.,-0.866025403784439));
#8802=DIRECTION('',(0.5,0.,0.866025403784439));
#8803=DIRECTION('',(0.,-1.,0.));
#8804=DIRECTION('',(-0.5,0.,-0.866025403784439));
#8805=DIRECTION('center_axis',(-2.40370335797945E-16,0.,1.));
#8806=DIRECTION('ref_axis',(-1.,0.,-2.40370335797945E-16));
#8807=DIRECTION('',(1.,0.,2.40370335797945E-16));
#8808=DIRECTION('',(0.,-1.,0.));
#8809=DIRECTION('',(-1.,0.,-2.40370335797945E-16));
#8810=DIRECTION('center_axis',(0.866025403784439,0.,0.5));
#8811=DIRECTION('ref_axis',(-0.5,0.,0.866025403784439));
#8812=DIRECTION('',(0.5,0.,-0.866025403784439));
#8813=DIRECTION('',(-0.5,0.,0.866025403784439));
#8814=DIRECTION('center_axis',(0.,1.,0.));
#8815=DIRECTION('ref_axis',(1.,0.,0.));
#8816=DIRECTION('center_axis',(0.,-1.,0.));
#8817=DIRECTION('ref_axis',(0.,0.,-1.));
#12354=CARTESIAN_POINT('',(0.,0.,0.));
#12355=CARTESIAN_POINT('Origin',(0.375,0.5,0.));
#12356=CARTESIAN_POINT('',(-0.375,0.5,-4.59242549680257E-17));
#12357=CARTESIAN_POINT('Origin',(0.,0.5,0.));
#12358=CARTESIAN_POINT('Origin',(0.,0.475,0.));
#12359=CARTESIAN_POINT('',(-0.425,0.45,-5.20474889637625E-17));
#12360=CARTESIAN_POINT('Origin',(0.,0.45,0.));
#12361=CARTESIAN_POINT('',(-0.4,0.475,-4.89858719658941E-17));
#12362=CARTESIAN_POINT('Origin',(0.,0.24,0.));
#12363=CARTESIAN_POINT('',(-0.425,0.0299999999999998,-5.20474889637625E-17));
#12364=CARTESIAN_POINT('Origin',(0.,0.0299999999999998,0.));
#12365=CARTESIAN_POINT('',(-0.425,0.24,-5.20474889637625E-17));
#12366=CARTESIAN_POINT('Origin',(0.,0.0150000000000001,0.));
#12367=CARTESIAN_POINT('',(-0.395,4.85722573273506E-17,-4.83735485663204E-17));
#12368=CARTESIAN_POINT('Origin',(0.,0.,0.));
#12369=CARTESIAN_POINT('',(-0.41,0.0150000000000001,-5.02105187650415E-17));
#12370=CARTESIAN_POINT('Origin',(0.27,0.,0.));
#12371=CARTESIAN_POINT('',(-0.27,0.,-3.30654635769785E-17));
#12372=CARTESIAN_POINT('Origin',(0.,0.,0.));
#12373=CARTESIAN_POINT('Origin',(0.,-0.02,0.));
#12374=CARTESIAN_POINT('',(-0.24505,-0.0498999999999999,3.00099698131059E-17));
#12375=CARTESIAN_POINT('Origin',(0.,-0.0498999999999999,0.));
#12376=CARTESIAN_POINT('',(-0.26,-0.02,-3.18408167778312E-17));
#12377=CARTESIAN_POINT('Origin',(0.,-0.995,0.));
#12378=CARTESIAN_POINT('',(-0.24505,-1.95495,3.00099698131059E-17));
#12379=CARTESIAN_POINT('Origin',(0.,-1.95495,0.));
#12380=CARTESIAN_POINT('',(-0.24505,-0.995,-3.00099698131059E-17));
#12381=CARTESIAN_POINT('Origin',(0.,-1.975,0.));
#12382=CARTESIAN_POINT('',(-0.2,-2.,-2.44929359829471E-17));
#12383=CARTESIAN_POINT('Origin',(0.,-2.,0.));
#12384=CARTESIAN_POINT('',(-0.225,-1.975,-2.75545529808154E-17));
#12385=CARTESIAN_POINT('Origin',(0.,-2.,0.));
#12386=CARTESIAN_POINT('Origin',(0.115470053837925,-0.5,-0.2));
#12387=CARTESIAN_POINT('',(0.23094010767585,-0.5,0.));
#12388=CARTESIAN_POINT('',(0.115470053837925,-0.5,-0.2));
#12389=CARTESIAN_POINT('',(0.23094010767585,-0.5,0.));
#12390=CARTESIAN_POINT('',(0.115470053837925,-0.8,-0.2));
#12391=CARTESIAN_POINT('',(0.115470053837925,-0.5,-0.2));
#12392=CARTESIAN_POINT('',(0.23094010767585,-0.8,0.));
#12393=CARTESIAN_POINT('',(0.23094010767585,-0.8,0.));
#12394=CARTESIAN_POINT('',(0.23094010767585,-0.5,0.));
#12395=CARTESIAN_POINT('Origin',(-0.115470053837925,-0.5,-0.2));
#12396=CARTESIAN_POINT('',(-0.115470053837925,-0.5,-0.2));
#12397=CARTESIAN_POINT('',(0.115470053837925,-0.5,-0.2));
#12398=CARTESIAN_POINT('',(-0.115470053837925,-0.8,-0.2));
#12399=CARTESIAN_POINT('',(-0.115470053837925,-0.5,-0.2));
#12400=CARTESIAN_POINT('',(0.115470053837925,-0.8,-0.2));
#12401=CARTESIAN_POINT('Origin',(-0.23094010767585,-0.5,-2.77555756156289E-17));
#12402=CARTESIAN_POINT('',(-0.23094010767585,-0.5,-2.82820063659975E-17));
#12403=CARTESIAN_POINT('',(-0.115470053837925,-0.5,-0.2));
#12404=CARTESIAN_POINT('',(-0.23094010767585,-0.8,-2.77555756156289E-17));
#12405=CARTESIAN_POINT('',(-0.23094010767585,-0.5,-2.82820063659975E-17));
#12406=CARTESIAN_POINT('',(-0.115470053837925,-0.8,-0.2));
#12407=CARTESIAN_POINT('Origin',(-0.115470053837925,-0.5,0.2));
#12408=CARTESIAN_POINT('',(-0.115470053837925,-0.5,0.2));
#12409=CARTESIAN_POINT('',(-0.23094010767585,-0.5,-2.82820063659975E-17));
#12410=CARTESIAN_POINT('',(-0.115470053837925,-0.8,0.2));
#12411=CARTESIAN_POINT('',(-0.115470053837925,-0.5,0.2));
#12412=CARTESIAN_POINT('',(-0.23094010767585,-0.8,-2.82820063659975E-17));
#12413=CARTESIAN_POINT('Origin',(0.115470053837925,-0.5,0.2));
#12414=CARTESIAN_POINT('',(0.115470053837925,-0.5,0.2));
#12415=CARTESIAN_POINT('',(-0.115470053837925,-0.5,0.2));
#12416=CARTESIAN_POINT('',(0.115470053837925,-0.8,0.2));
#12417=CARTESIAN_POINT('',(0.115470053837925,-0.5,0.2));
#12418=CARTESIAN_POINT('',(-0.115470053837925,-0.8,0.2));
#12419=CARTESIAN_POINT('Origin',(0.23094010767585,-0.5,0.));
#12420=CARTESIAN_POINT('',(0.115470053837925,-0.5,0.2));
#12421=CARTESIAN_POINT('',(0.115470053837925,-0.8,0.2));
#12422=CARTESIAN_POINT('Origin',(0.,-0.5,0.));
#12423=CARTESIAN_POINT('Origin',(0.,-0.8,0.));
#13211=UNCERTAINTY_MEASURE_WITH_UNIT(LENGTH_MEASURE(0.001),#13278,
'DISTANCE_ACCURACY_VALUE',
'Maximum model space distance between geometric entities at asserted c
onnectivities');
#13233=UNCERTAINTY_MEASURE_WITH_UNIT(LENGTH_MEASURE(0.001),#13278,
'DISTANCE_ACCURACY_VALUE',
'Maximum model space distance between geometric entities at asserted c
onnectivities');
#13255=(
GEOMETRIC_REPRESENTATION_CONTEXT(3)
GLOBAL_UNCERTAINTY_ASSIGNED_CONTEXT((#13211))
GLOBAL_UNIT_ASSIGNED_CONTEXT((#13278,#13280,#13281))
REPRESENTATION_CONTEXT('','3D')
);
#13277=(
GEOMETRIC_REPRESENTATION_CONTEXT(3)
GLOBAL_UNCERTAINTY_ASSIGNED_CONTEXT((#13233))
GLOBAL_UNIT_ASSIGNED_CONTEXT((#13278,#13280,#13281))
REPRESENTATION_CONTEXT('','3D')
);
#13278=(
LENGTH_UNIT()
NAMED_UNIT(*)
SI_UNIT(.CENTI.,.METRE.)
);
#13280=(
NAMED_UNIT(*)
PLANE_ANGLE_UNIT()
SI_UNIT($,.RADIAN.)
);
#13281=(
NAMED_UNIT(*)
SI_UNIT($,.STERADIAN.)
SOLID_ANGLE_UNIT()
);
#13303=SHAPE_DEFINITION_REPRESENTATION(#13351,#13460);
#13351=PRODUCT_DEFINITION_SHAPE('',$,#13504);
#13460=SHAPE_REPRESENTATION('',(#7282),#13255);
#13482=PRODUCT_DEFINITION_CONTEXT('part definition',#13613,'design');
#13504=PRODUCT_DEFINITION('Cap Screw - M5x20','Cap Screw - M5x20',#13547,
#13482);
#13547=PRODUCT_DEFINITION_FORMATION('',$,#13636);
#13613=APPLICATION_CONTEXT(
'Core Data for Automotive Mechanical Design Process');
#13614=PRODUCT_CONTEXT('part definition',#13613,'mechanical');
#13636=PRODUCT('Cap Screw - M5x20','Cap Screw - M5x20',
'Cap Screw - M5x20',(#13614));
#13721=COLOUR_RGB('Black',0.12,0.14,0.17);
#13722=FILL_AREA_STYLE_COLOUR('',#13721);
#13723=FILL_AREA_STYLE('',(#13722));
#13724=SURFACE_STYLE_FILL_AREA(#13723);
#13725=SURFACE_SIDE_STYLE('',(#13724));
#13726=SURFACE_STYLE_USAGE(.BOTH.,#13725);
#13727=PRESENTATION_STYLE_ASSIGNMENT((#13726));
ENDSEC;
END-ISO-10303-21;
